ISO-10303-21;
HEADER;
/* Generated by software containing ST-Developer
 * from STEP Tools, Inc. (www.steptools.com) 
 */

FILE_DESCRIPTION(
/* description */ ('Bell-crank linkage with push rods'),
/* implementation_level */ '2;1');

FILE_NAME(
/* name */ 'Vertical shaft support (1).step',
/* time_stamp */ '2026-10-28T03:25:15-07:00',
/* author */ (''),
/* organization */ (''),
/* preprocessor_version */ 'ST-DEVELOPER v20.2',
/* originating_system */ 'Autodesk Translation Framework v15.17.0.0',
/* authorisation */ '');

FILE_SCHEMA (('AUTOMOTIVE_DESIGN { 1 0 10303 214 3 1 1 }'));
ENDSEC;

DATA;
#10=MECHANICAL_DESIGN_GEOMETRIC_PRESENTATION_REPRESENTATION('',(#612),#16678);
#471=B_SPLINE_CURVE_WITH_KNOTS('',3,(#14321,#14322,#14323,#14324,#14325,
#14326,#14327,#14328,#14329,#14330),.UNSPECIFIED.,.F.,.F.,(4,2,2,2,4),(0.635430324955933,
0.687528937234029,0.750024497760674,0.81252005828732,0.86461867056541),
 .UNSPECIFIED.);
#472=B_SPLINE_CURVE_WITH_KNOTS('',3,(#14338,#14339,#14340,#14341,#14342,
#14343,#14344,#14345,#14346,#14347),.UNSPECIFIED.,.F.,.F.,(4,2,2,2,4),(0.135413993115484,
0.187512605393579,0.250008165920225,0.31250372644687,0.364602338724967),
 .UNSPECIFIED.);
#504=SHAPE_REPRESENTATION_RELATIONSHIP('SRR','None',#16920,#558);
#558=ADVANCED_BREP_SHAPE_REPRESENTATION('',(#674),#16625);
#612=STYLED_ITEM('',(#17291),#674);
#674=MANIFOLD_SOLID_BREP('Body1',#8802);
#804=FACE_BOUND('',#1984,.T.);
#805=FACE_BOUND('',#1987,.T.);
#806=FACE_BOUND('',#1989,.T.);
#807=FACE_BOUND('',#1993,.T.);
#808=FACE_BOUND('',#1995,.T.);
#809=FACE_BOUND('',#1998,.T.);
#810=FACE_BOUND('',#2001,.T.);
#811=FACE_BOUND('',#2002,.T.);
#1033=PLANE('',#9734);
#1034=PLANE('',#9740);
#1035=PLANE('',#9744);
#1036=PLANE('',#9749);
#1037=PLANE('',#9751);
#1038=PLANE('',#9759);
#1039=PLANE('',#9760);
#1040=PLANE('',#9761);
#1041=PLANE('',#9762);
#1042=PLANE('',#9763);
#1377=FACE_OUTER_BOUND('',#1978,.T.);
#1378=FACE_OUTER_BOUND('',#1979,.T.);
#1379=FACE_OUTER_BOUND('',#1980,.T.);
#1380=FACE_OUTER_BOUND('',#1981,.T.);
#1381=FACE_OUTER_BOUND('',#1982,.T.);
#1382=FACE_OUTER_BOUND('',#1983,.T.);
#1383=FACE_OUTER_BOUND('',#1985,.T.);
#1384=FACE_OUTER_BOUND('',#1986,.T.);
#1385=FACE_OUTER_BOUND('',#1988,.T.);
#1386=FACE_OUTER_BOUND('',#1990,.T.);
#1387=FACE_OUTER_BOUND('',#1991,.T.);
#1388=FACE_OUTER_BOUND('',#1992,.T.);
#1389=FACE_OUTER_BOUND('',#1994,.T.);
#1390=FACE_OUTER_BOUND('',#1996,.T.);
#1391=FACE_OUTER_BOUND('',#1997,.T.);
#1392=FACE_OUTER_BOUND('',#1999,.T.);
#1393=FACE_OUTER_BOUND('',#2000,.T.);
#1978=EDGE_LOOP('',(#6529,#6530,#6531,#6532));
#1979=EDGE_LOOP('',(#6533,#6534));
#1980=EDGE_LOOP('',(#6535,#6536,#6537,#6538,#6539,#6540,#6541,#6542));
#1981=EDGE_LOOP('',(#6543,#6544,#6545));
#1982=EDGE_LOOP('',(#6546,#6547,#6548,#6549));
#1983=EDGE_LOOP('',(#6550));
#1984=EDGE_LOOP('',(#6551));
#1985=EDGE_LOOP('',(#6552,#6553,#6554,#6555));
#1986=EDGE_LOOP('',(#6556,#6557));
#1987=EDGE_LOOP('',(#6558));
#1988=EDGE_LOOP('',(#6559,#6560,#6561,#6562,#6563,#6564,#6565,#6566,#6567));
#1989=EDGE_LOOP('',(#6568));
#1990=EDGE_LOOP('',(#6569,#6570,#6571,#6572));
#1991=EDGE_LOOP('',(#6573,#6574,#6575,#6576));
#1992=EDGE_LOOP('',(#6577,#6578,#6579,#6580));
#1993=EDGE_LOOP('',(#6581,#6582,#6583,#6584));
#1994=EDGE_LOOP('',(#6585,#6586,#6587,#6588));
#1995=EDGE_LOOP('',(#6589));
#1996=EDGE_LOOP('',(#6590,#6591,#6592,#6593,#6594,#6595,#6596));
#1997=EDGE_LOOP('',(#6597,#6598,#6599,#6600));
#1998=EDGE_LOOP('',(#6601));
#1999=EDGE_LOOP('',(#6602,#6603,#6604,#6605,#6606,#6607,#6608));
#2000=EDGE_LOOP('',(#6609,#6610,#6611,#6612));
#2001=EDGE_LOOP('',(#6613));
#2002=EDGE_LOOP('',(#6614));
#2691=LINE('',#14308,#3240);
#2692=LINE('',#14312,#3241);
#2693=LINE('',#14317,#3242);
#2694=LINE('',#14334,#3243);
#2695=LINE('',#14349,#3244);
#2696=LINE('',#14354,#3245);
#2697=LINE('',#14356,#3246);
#2698=LINE('',#14362,#3247);
#2699=LINE('',#14369,#3248);
#2700=LINE('',#14371,#3249);
#2701=LINE('',#14373,#3250);
#2702=LINE('',#14374,#3251);
#2703=LINE('',#14376,#3252);
#2704=LINE('',#14377,#3253);
#2705=LINE('',#14381,#3254);
#2706=LINE('',#14385,#3255);
#2707=LINE('',#14390,#3256);
#2708=LINE('',#14395,#3257);
#2709=LINE('',#14396,#3258);
#2710=LINE('',#14397,#3259);
#2711=LINE('',#14400,#3260);
#2712=LINE('',#14401,#3261);
#2713=LINE('',#14404,#3262);
#2714=LINE('',#14405,#3263);
#2715=LINE('',#14407,#3264);
#3240=VECTOR('',#11345,0.4);
#3241=VECTOR('',#11348,1.);
#3242=VECTOR('',#11353,1.);
#3243=VECTOR('',#11360,0.165);
#3244=VECTOR('',#11367,1.);
#3245=VECTOR('',#11372,1.);
#3246=VECTOR('',#11375,1.);
#3247=VECTOR('',#11384,1.);
#3248=VECTOR('',#11393,1.);
#3249=VECTOR('',#11394,1.);
#3250=VECTOR('',#11395,1.);
#3251=VECTOR('',#11396,1.);
#3252=VECTOR('',#11397,1.);
#3253=VECTOR('',#11398,1.);
#3254=VECTOR('',#11403,0.225);
#3255=VECTOR('',#11408,0.225);
#3256=VECTOR('',#11413,0.6);
#3257=VECTOR('',#11418,1.);
#3258=VECTOR('',#11419,1.);
#3259=VECTOR('',#11420,1.);
#3260=VECTOR('',#11423,1.);
#3261=VECTOR('',#11424,1.);
#3262=VECTOR('',#11427,1.);
#3263=VECTOR('',#11428,1.);
#3264=VECTOR('',#11431,1.);
#3766=CIRCLE('',#9732,0.4);
#3767=CIRCLE('',#9733,0.4);
#3768=CIRCLE('',#9735,0.165);
#3769=CIRCLE('',#9737,0.165);
#3770=CIRCLE('',#9738,0.165);
#3771=CIRCLE('',#9739,0.165);
#3772=CIRCLE('',#9742,0.4);
#3773=CIRCLE('',#9743,0.4);
#3774=CIRCLE('',#9745,0.225);
#3775=CIRCLE('',#9747,0.4);
#3776=CIRCLE('',#9748,0.4);
#3777=CIRCLE('',#9750,0.225);
#3778=CIRCLE('',#9753,0.225);
#3779=CIRCLE('',#9755,0.225);
#3780=CIRCLE('',#9757,0.6);
#3781=CIRCLE('',#9758,0.6);
#4318=VERTEX_POINT('',#14306);
#4319=VERTEX_POINT('',#14307);
#4320=VERTEX_POINT('',#14309);
#4321=VERTEX_POINT('',#14311);
#4322=VERTEX_POINT('',#14315);
#4323=VERTEX_POINT('',#14316);
#4324=VERTEX_POINT('',#14320);
#4325=VERTEX_POINT('',#14331);
#4326=VERTEX_POINT('',#14333);
#4327=VERTEX_POINT('',#14336);
#4328=VERTEX_POINT('',#14351);
#4329=VERTEX_POINT('',#14353);
#4330=VERTEX_POINT('',#14358);
#4331=VERTEX_POINT('',#14365);
#4332=VERTEX_POINT('',#14368);
#4333=VERTEX_POINT('',#14370);
#4334=VERTEX_POINT('',#14372);
#4335=VERTEX_POINT('',#14375);
#4336=VERTEX_POINT('',#14379);
#4337=VERTEX_POINT('',#14383);
#4338=VERTEX_POINT('',#14387);
#4339=VERTEX_POINT('',#14389);
#4340=VERTEX_POINT('',#14393);
#4341=VERTEX_POINT('',#14394);
#4342=VERTEX_POINT('',#14399);
#4343=VERTEX_POINT('',#14403);
#5142=EDGE_CURVE('',#4318,#4319,#2691,.T.);
#5143=EDGE_CURVE('',#4320,#4318,#3766,.T.);
#5144=EDGE_CURVE('',#4320,#4321,#2692,.T.);
#5145=EDGE_CURVE('',#4319,#4321,#3767,.T.);
#5146=EDGE_CURVE('',#4322,#4323,#2693,.T.);
#5147=EDGE_CURVE('',#4322,#4323,#3768,.T.);
#5148=EDGE_CURVE('',#4324,#4322,#471,.T.);
#5149=EDGE_CURVE('',#4325,#4324,#3769,.T.);
#5150=EDGE_CURVE('',#4325,#4326,#2694,.T.);
#5151=EDGE_CURVE('',#4326,#4326,#3770,.T.);
#5152=EDGE_CURVE('',#4327,#4325,#3771,.T.);
#5153=EDGE_CURVE('',#4323,#4327,#472,.T.);
#5154=EDGE_CURVE('',#4327,#4324,#2695,.T.);
#5155=EDGE_CURVE('',#4328,#4328,#3772,.T.);
#5156=EDGE_CURVE('',#4328,#4329,#2696,.T.);
#5157=EDGE_CURVE('',#4329,#4329,#3773,.T.);
#5158=EDGE_CURVE('',#4328,#4329,#2697,.T.);
#5159=EDGE_CURVE('',#4330,#4330,#3774,.T.);
#5160=EDGE_CURVE('',#4321,#4319,#3775,.T.);
#5161=EDGE_CURVE('',#4320,#4321,#2698,.T.);
#5162=EDGE_CURVE('',#4318,#4320,#3776,.T.);
#5163=EDGE_CURVE('',#4331,#4331,#3777,.T.);
#5164=EDGE_CURVE('',#4332,#4329,#2699,.T.);
#5165=EDGE_CURVE('',#4329,#4333,#2700,.T.);
#5166=EDGE_CURVE('',#4333,#4334,#2701,.T.);
#5167=EDGE_CURVE('',#4334,#4321,#2702,.T.);
#5168=EDGE_CURVE('',#4321,#4335,#2703,.T.);
#5169=EDGE_CURVE('',#4335,#4332,#2704,.T.);
#5170=EDGE_CURVE('',#4336,#4336,#3778,.T.);
#5171=EDGE_CURVE('',#4336,#4330,#2705,.T.);
#5172=EDGE_CURVE('',#4337,#4337,#3779,.T.);
#5173=EDGE_CURVE('',#4337,#4331,#2706,.T.);
#5174=EDGE_CURVE('',#4338,#4338,#3780,.T.);
#5175=EDGE_CURVE('',#4338,#4339,#2707,.T.);
#5176=EDGE_CURVE('',#4339,#4339,#3781,.T.);
#5177=EDGE_CURVE('',#4340,#4341,#2708,.T.);
#5178=EDGE_CURVE('',#4341,#4332,#2709,.T.);
#5179=EDGE_CURVE('',#4340,#4335,#2710,.T.);
#5180=EDGE_CURVE('',#4342,#4340,#2711,.T.);
#5181=EDGE_CURVE('',#4342,#4334,#2712,.T.);
#5182=EDGE_CURVE('',#4343,#4342,#2713,.T.);
#5183=EDGE_CURVE('',#4343,#4333,#2714,.T.);
#5184=EDGE_CURVE('',#4341,#4343,#2715,.T.);
#6529=ORIENTED_EDGE('',*,*,#5142,.F.);
#6530=ORIENTED_EDGE('',*,*,#5143,.F.);
#6531=ORIENTED_EDGE('',*,*,#5144,.T.);
#6532=ORIENTED_EDGE('',*,*,#5145,.F.);
#6533=ORIENTED_EDGE('',*,*,#5146,.F.);
#6534=ORIENTED_EDGE('',*,*,#5147,.T.);
#6535=ORIENTED_EDGE('',*,*,#5148,.F.);
#6536=ORIENTED_EDGE('',*,*,#5149,.F.);
#6537=ORIENTED_EDGE('',*,*,#5150,.T.);
#6538=ORIENTED_EDGE('',*,*,#5151,.F.);
#6539=ORIENTED_EDGE('',*,*,#5150,.F.);
#6540=ORIENTED_EDGE('',*,*,#5152,.F.);
#6541=ORIENTED_EDGE('',*,*,#5153,.F.);
#6542=ORIENTED_EDGE('',*,*,#5147,.F.);
#6543=ORIENTED_EDGE('',*,*,#5154,.F.);
#6544=ORIENTED_EDGE('',*,*,#5152,.T.);
#6545=ORIENTED_EDGE('',*,*,#5149,.T.);
#6546=ORIENTED_EDGE('',*,*,#5155,.F.);
#6547=ORIENTED_EDGE('',*,*,#5156,.T.);
#6548=ORIENTED_EDGE('',*,*,#5157,.F.);
#6549=ORIENTED_EDGE('',*,*,#5158,.F.);
#6550=ORIENTED_EDGE('',*,*,#5155,.T.);
#6551=ORIENTED_EDGE('',*,*,#5159,.F.);
#6552=ORIENTED_EDGE('',*,*,#5142,.T.);
#6553=ORIENTED_EDGE('',*,*,#5160,.F.);
#6554=ORIENTED_EDGE('',*,*,#5161,.F.);
#6555=ORIENTED_EDGE('',*,*,#5162,.F.);
#6556=ORIENTED_EDGE('',*,*,#5143,.T.);
#6557=ORIENTED_EDGE('',*,*,#5162,.T.);
#6558=ORIENTED_EDGE('',*,*,#5163,.F.);
#6559=ORIENTED_EDGE('',*,*,#5164,.T.);
#6560=ORIENTED_EDGE('',*,*,#5157,.T.);
#6561=ORIENTED_EDGE('',*,*,#5165,.T.);
#6562=ORIENTED_EDGE('',*,*,#5166,.T.);
#6563=ORIENTED_EDGE('',*,*,#5167,.T.);
#6564=ORIENTED_EDGE('',*,*,#5160,.T.);
#6565=ORIENTED_EDGE('',*,*,#5145,.T.);
#6566=ORIENTED_EDGE('',*,*,#5168,.T.);
#6567=ORIENTED_EDGE('',*,*,#5169,.T.);
#6568=ORIENTED_EDGE('',*,*,#5151,.T.);
#6569=ORIENTED_EDGE('',*,*,#5170,.F.);
#6570=ORIENTED_EDGE('',*,*,#5171,.T.);
#6571=ORIENTED_EDGE('',*,*,#5159,.T.);
#6572=ORIENTED_EDGE('',*,*,#5171,.F.);
#6573=ORIENTED_EDGE('',*,*,#5172,.F.);
#6574=ORIENTED_EDGE('',*,*,#5173,.T.);
#6575=ORIENTED_EDGE('',*,*,#5163,.T.);
#6576=ORIENTED_EDGE('',*,*,#5173,.F.);
#6577=ORIENTED_EDGE('',*,*,#5174,.F.);
#6578=ORIENTED_EDGE('',*,*,#5175,.T.);
#6579=ORIENTED_EDGE('',*,*,#5176,.F.);
#6580=ORIENTED_EDGE('',*,*,#5175,.F.);
#6581=ORIENTED_EDGE('',*,*,#5153,.T.);
#6582=ORIENTED_EDGE('',*,*,#5154,.T.);
#6583=ORIENTED_EDGE('',*,*,#5148,.T.);
#6584=ORIENTED_EDGE('',*,*,#5146,.T.);
#6585=ORIENTED_EDGE('',*,*,#5177,.T.);
#6586=ORIENTED_EDGE('',*,*,#5178,.T.);
#6587=ORIENTED_EDGE('',*,*,#5169,.F.);
#6588=ORIENTED_EDGE('',*,*,#5179,.F.);
#6589=ORIENTED_EDGE('',*,*,#5176,.T.);
#6590=ORIENTED_EDGE('',*,*,#5180,.T.);
#6591=ORIENTED_EDGE('',*,*,#5179,.T.);
#6592=ORIENTED_EDGE('',*,*,#5168,.F.);
#6593=ORIENTED_EDGE('',*,*,#5144,.F.);
#6594=ORIENTED_EDGE('',*,*,#5161,.T.);
#6595=ORIENTED_EDGE('',*,*,#5167,.F.);
#6596=ORIENTED_EDGE('',*,*,#5181,.F.);
#6597=ORIENTED_EDGE('',*,*,#5182,.T.);
#6598=ORIENTED_EDGE('',*,*,#5181,.T.);
#6599=ORIENTED_EDGE('',*,*,#5166,.F.);
#6600=ORIENTED_EDGE('',*,*,#5183,.F.);
#6601=ORIENTED_EDGE('',*,*,#5174,.T.);
#6602=ORIENTED_EDGE('',*,*,#5184,.T.);
#6603=ORIENTED_EDGE('',*,*,#5183,.T.);
#6604=ORIENTED_EDGE('',*,*,#5165,.F.);
#6605=ORIENTED_EDGE('',*,*,#5156,.F.);
#6606=ORIENTED_EDGE('',*,*,#5158,.T.);
#6607=ORIENTED_EDGE('',*,*,#5164,.F.);
#6608=ORIENTED_EDGE('',*,*,#5178,.F.);
#6609=ORIENTED_EDGE('',*,*,#5184,.F.);
#6610=ORIENTED_EDGE('',*,*,#5177,.F.);
#6611=ORIENTED_EDGE('',*,*,#5180,.F.);
#6612=ORIENTED_EDGE('',*,*,#5182,.F.);
#6613=ORIENTED_EDGE('',*,*,#5170,.T.);
#6614=ORIENTED_EDGE('',*,*,#5172,.T.);
#8130=CYLINDRICAL_SURFACE('',#9731,0.4);
#8131=CYLINDRICAL_SURFACE('',#9736,0.165);
#8132=CYLINDRICAL_SURFACE('',#9741,0.4);
#8133=CYLINDRICAL_SURFACE('',#9746,0.4);
#8134=CYLINDRICAL_SURFACE('',#9752,0.225);
#8135=CYLINDRICAL_SURFACE('',#9754,0.225);
#8136=CYLINDRICAL_SURFACE('',#9756,0.6);
#8402=ADVANCED_FACE('',(#1377),#8130,.F.);
#8403=ADVANCED_FACE('',(#1378),#1033,.T.);
#8404=ADVANCED_FACE('',(#1379),#8131,.F.);
#8405=ADVANCED_FACE('',(#1380),#1034,.T.);
#8406=ADVANCED_FACE('',(#1381),#8132,.F.);
#8407=ADVANCED_FACE('',(#1382,#804),#1035,.T.);
#8408=ADVANCED_FACE('',(#1383),#8133,.F.);
#8409=ADVANCED_FACE('',(#1384,#805),#1036,.T.);
#8410=ADVANCED_FACE('',(#1385,#806),#1037,.T.);
#8411=ADVANCED_FACE('',(#1386),#8134,.F.);
#8412=ADVANCED_FACE('',(#1387),#8135,.F.);
#8413=ADVANCED_FACE('',(#1388,#807),#8136,.F.);
#8414=ADVANCED_FACE('',(#1389,#808),#1038,.T.);
#8415=ADVANCED_FACE('',(#1390),#1039,.T.);
#8416=ADVANCED_FACE('',(#1391,#809),#1040,.T.);
#8417=ADVANCED_FACE('',(#1392),#1041,.T.);
#8418=ADVANCED_FACE('',(#1393,#810,#811),#1042,.F.);
#8802=CLOSED_SHELL('',(#8402,#8403,#8404,#8405,#8406,#8407,#8408,#8409,
#8410,#8411,#8412,#8413,#8414,#8415,#8416,#8417,#8418));
#9730=AXIS2_PLACEMENT_3D('',#14304,#11341,#11342);
#9731=AXIS2_PLACEMENT_3D('',#14305,#11343,#11344);
#9732=AXIS2_PLACEMENT_3D('',#14310,#11346,#11347);
#9733=AXIS2_PLACEMENT_3D('',#14313,#11349,#11350);
#9734=AXIS2_PLACEMENT_3D('',#14314,#11351,#11352);
#9735=AXIS2_PLACEMENT_3D('',#14318,#11354,#11355);
#9736=AXIS2_PLACEMENT_3D('',#14319,#11356,#11357);
#9737=AXIS2_PLACEMENT_3D('',#14332,#11358,#11359);
#9738=AXIS2_PLACEMENT_3D('',#14335,#11361,#11362);
#9739=AXIS2_PLACEMENT_3D('',#14337,#11363,#11364);
#9740=AXIS2_PLACEMENT_3D('',#14348,#11365,#11366);
#9741=AXIS2_PLACEMENT_3D('',#14350,#11368,#11369);
#9742=AXIS2_PLACEMENT_3D('',#14352,#11370,#11371);
#9743=AXIS2_PLACEMENT_3D('',#14355,#11373,#11374);
#9744=AXIS2_PLACEMENT_3D('',#14357,#11376,#11377);
#9745=AXIS2_PLACEMENT_3D('',#14359,#11378,#11379);
#9746=AXIS2_PLACEMENT_3D('',#14360,#11380,#11381);
#9747=AXIS2_PLACEMENT_3D('',#14361,#11382,#11383);
#9748=AXIS2_PLACEMENT_3D('',#14363,#11385,#11386);
#9749=AXIS2_PLACEMENT_3D('',#14364,#11387,#11388);
#9750=AXIS2_PLACEMENT_3D('',#14366,#11389,#11390);
#9751=AXIS2_PLACEMENT_3D('',#14367,#11391,#11392);
#9752=AXIS2_PLACEMENT_3D('',#14378,#11399,#11400);
#9753=AXIS2_PLACEMENT_3D('',#14380,#11401,#11402);
#9754=AXIS2_PLACEMENT_3D('',#14382,#11404,#11405);
#9755=AXIS2_PLACEMENT_3D('',#14384,#11406,#11407);
#9756=AXIS2_PLACEMENT_3D('',#14386,#11409,#11410);
#9757=AXIS2_PLACEMENT_3D('',#14388,#11411,#11412);
#9758=AXIS2_PLACEMENT_3D('',#14391,#11414,#11415);
#9759=AXIS2_PLACEMENT_3D('',#14392,#11416,#11417);
#9760=AXIS2_PLACEMENT_3D('',#14398,#11421,#11422);
#9761=AXIS2_PLACEMENT_3D('',#14402,#11425,#11426);
#9762=AXIS2_PLACEMENT_3D('',#14406,#11429,#11430);
#9763=AXIS2_PLACEMENT_3D('',#14408,#11432,#11433);
#11341=DIRECTION('axis',(0.,0.,1.));
#11342=DIRECTION('refdir',(1.,0.,0.));
#11343=DIRECTION('center_axis',(0.,0.,1.));
#11344=DIRECTION('ref_axis',(1.,0.,0.));
#11345=DIRECTION('',(0.,0.,1.));
#11346=DIRECTION('center_axis',(0.,0.,1.));
#11347=DIRECTION('ref_axis',(1.,0.,0.));
#11348=DIRECTION('',(0.,0.,1.));
#11349=DIRECTION('center_axis',(0.,0.,-1.));
#11350=DIRECTION('ref_axis',(1.,0.,0.));
#11351=DIRECTION('center_axis',(0.,0.,1.));
#11352=DIRECTION('ref_axis',(1.,0.,0.));
#11353=DIRECTION('',(0.,1.,0.));
#11354=DIRECTION('center_axis',(0.,0.,1.));
#11355=DIRECTION('ref_axis',(1.,0.,0.));
#11356=DIRECTION('center_axis',(0.,0.,1.));
#11357=DIRECTION('ref_axis',(1.,0.,0.));
#11358=DIRECTION('center_axis',(0.,0.,1.));
#11359=DIRECTION('ref_axis',(1.,0.,0.));
#11360=DIRECTION('',(0.,0.,1.));
#11361=DIRECTION('center_axis',(0.,0.,-1.));
#11362=DIRECTION('ref_axis',(1.,0.,0.));
#11363=DIRECTION('center_axis',(0.,0.,1.));
#11364=DIRECTION('ref_axis',(1.,0.,0.));
#11365=DIRECTION('center_axis',(0.,0.,1.));
#11366=DIRECTION('ref_axis',(1.,0.,0.));
#11367=DIRECTION('',(0.,-1.,0.));
#11368=DIRECTION('center_axis',(0.,0.,1.));
#11369=DIRECTION('ref_axis',(1.,0.,0.));
#11370=DIRECTION('center_axis',(0.,0.,1.));
#11371=DIRECTION('ref_axis',(1.,0.,0.));
#11372=DIRECTION('',(0.,0.,1.));
#11373=DIRECTION('center_axis',(0.,0.,-1.));
#11374=DIRECTION('ref_axis',(1.,0.,0.));
#11375=DIRECTION('',(0.,0.,1.));
#11376=DIRECTION('center_axis',(0.,0.,1.));
#11377=DIRECTION('ref_axis',(1.,0.,0.));
#11378=DIRECTION('center_axis',(0.,0.,1.));
#11379=DIRECTION('ref_axis',(1.,0.,0.));
#11380=DIRECTION('center_axis',(0.,0.,1.));
#11381=DIRECTION('ref_axis',(1.,0.,0.));
#11382=DIRECTION('center_axis',(0.,0.,-1.));
#11383=DIRECTION('ref_axis',(1.,0.,0.));
#11384=DIRECTION('',(0.,0.,1.));
#11385=DIRECTION('center_axis',(0.,0.,1.));
#11386=DIRECTION('ref_axis',(1.,0.,0.));
#11387=DIRECTION('center_axis',(0.,0.,1.));
#11388=DIRECTION('ref_axis',(1.,0.,0.));
#11389=DIRECTION('center_axis',(0.,0.,1.));
#11390=DIRECTION('ref_axis',(1.,0.,0.));
#11391=DIRECTION('center_axis',(0.,0.,1.));
#11392=DIRECTION('ref_axis',(1.,0.,0.));
#11393=DIRECTION('',(0.,-1.,0.));
#11394=DIRECTION('',(0.,-1.,0.));
#11395=DIRECTION('',(1.,0.,0.));
#11396=DIRECTION('',(0.,1.,0.));
#11397=DIRECTION('',(0.,1.,0.));
#11398=DIRECTION('',(-1.,0.,0.));
#11399=DIRECTION('center_axis',(0.,0.,1.));
#11400=DIRECTION('ref_axis',(1.,0.,0.));
#11401=DIRECTION('center_axis',(0.,0.,1.));
#11402=DIRECTION('ref_axis',(1.,0.,0.));
#11403=DIRECTION('',(0.,0.,1.));
#11404=DIRECTION('center_axis',(0.,0.,1.));
#11405=DIRECTION('ref_axis',(1.,0.,0.));
#11406=DIRECTION('center_axis',(0.,0.,1.));
#11407=DIRECTION('ref_axis',(1.,0.,0.));
#11408=DIRECTION('',(0.,0.,1.));
#11409=DIRECTION('center_axis',(0.,1.,0.));
#11410=DIRECTION('ref_axis',(1.,0.,0.));
#11411=DIRECTION('center_axis',(0.,1.,0.));
#11412=DIRECTION('ref_axis',(1.,0.,0.));
#11413=DIRECTION('',(0.,1.,0.));
#11414=DIRECTION('center_axis',(0.,-1.,0.));
#11415=DIRECTION('ref_axis',(1.,0.,0.));
#11416=DIRECTION('center_axis',(0.,1.,0.));
#11417=DIRECTION('ref_axis',(-1.,0.,0.));
#11418=DIRECTION('',(-1.,0.,0.));
#11419=DIRECTION('',(0.,0.,1.));
#11420=DIRECTION('',(0.,0.,1.));
#11421=DIRECTION('center_axis',(1.,0.,0.));
#11422=DIRECTION('ref_axis',(0.,1.,0.));
#11423=DIRECTION('',(0.,1.,0.));
#11424=DIRECTION('',(0.,0.,1.));
#11425=DIRECTION('center_axis',(0.,-1.,0.));
#11426=DIRECTION('ref_axis',(1.,0.,0.));
#11427=DIRECTION('',(1.,0.,0.));
#11428=DIRECTION('',(0.,0.,1.));
#11429=DIRECTION('center_axis',(-1.,0.,0.));
#11430=DIRECTION('ref_axis',(0.,-1.,0.));
#11431=DIRECTION('',(0.,-1.,0.));
#11432=DIRECTION('center_axis',(0.,0.,1.));
#11433=DIRECTION('ref_axis',(1.,0.,0.));
#14304=CARTESIAN_POINT('',(0.,0.,0.));
#14305=CARTESIAN_POINT('Origin',(5.1,17.5,2.));
#14306=CARTESIAN_POINT('',(4.7,17.5,2.));
#14307=CARTESIAN_POINT('',(4.7,17.5,5.));
#14308=CARTESIAN_POINT('',(4.7,17.5,2.));
#14309=CARTESIAN_POINT('',(5.5,17.5,2.));
#14310=CARTESIAN_POINT('Origin',(5.1,17.5,2.));
#14311=CARTESIAN_POINT('',(5.5,17.5,5.));
#14312=CARTESIAN_POINT('',(5.5,17.5,2.));
#14313=CARTESIAN_POINT('Origin',(5.1,17.5,5.));
#14314=CARTESIAN_POINT('Origin',(4.,17.5,4.59));
#14315=CARTESIAN_POINT('',(4.10908712114636,17.3762058159686,4.59));
#14316=CARTESIAN_POINT('',(4.10908712114636,17.6237941840314,4.59));
#14317=CARTESIAN_POINT('',(4.10908712114636,16.9,4.59));
#14318=CARTESIAN_POINT('Origin',(4.,17.5,4.59));
#14319=CARTESIAN_POINT('Origin',(4.,17.5,4.59));
#14320=CARTESIAN_POINT('',(3.89091287885364,17.3762058159686,4.59));
#14321=CARTESIAN_POINT('Ctrl Pts',(3.89091287885364,17.3762058159686,4.59));
#14322=CARTESIAN_POINT('Ctrl Pts',(3.90408240284739,17.3646008648105,4.59243495840567));
#14323=CARTESIAN_POINT('Ctrl Pts',(3.91977655056228,17.3546543563418,4.59485638705045));
#14324=CARTESIAN_POINT('Ctrl Pts',(3.95701983403981,17.339185135366,4.59880705606552));
#14325=CARTESIAN_POINT('Ctrl Pts',(3.97916814649112,17.335,4.6));
#14326=CARTESIAN_POINT('Ctrl Pts',(4.02083185350888,17.335,4.6));
#14327=CARTESIAN_POINT('Ctrl Pts',(4.04298016596019,17.339185135366,4.59880705606552));
#14328=CARTESIAN_POINT('Ctrl Pts',(4.08022344943772,17.3546543563418,4.59485638705045));
#14329=CARTESIAN_POINT('Ctrl Pts',(4.09591759715261,17.3646008648105,4.59243495840567));
#14330=CARTESIAN_POINT('Ctrl Pts',(4.10908712114636,17.3762058159686,4.59));
#14331=CARTESIAN_POINT('',(3.835,17.5,4.59));
#14332=CARTESIAN_POINT('Origin',(4.,17.5,4.59));
#14333=CARTESIAN_POINT('',(3.835,17.5,5.));
#14334=CARTESIAN_POINT('',(3.835,17.5,4.59));
#14335=CARTESIAN_POINT('Origin',(4.,17.5,5.));
#14336=CARTESIAN_POINT('',(3.89091287885364,17.6237941840314,4.59));
#14337=CARTESIAN_POINT('Origin',(4.,17.5,4.59));
#14338=CARTESIAN_POINT('Ctrl Pts',(4.10908712114636,17.6237941840314,4.59));
#14339=CARTESIAN_POINT('Ctrl Pts',(4.09591759715261,17.6353991351895,4.59243495840567));
#14340=CARTESIAN_POINT('Ctrl Pts',(4.08022344943772,17.6453456436582,4.59485638705045));
#14341=CARTESIAN_POINT('Ctrl Pts',(4.04298016596019,17.660814864634,4.59880705606552));
#14342=CARTESIAN_POINT('Ctrl Pts',(4.02083185350888,17.665,4.6));
#14343=CARTESIAN_POINT('Ctrl Pts',(3.97916814649112,17.665,4.6));
#14344=CARTESIAN_POINT('Ctrl Pts',(3.95701983403981,17.660814864634,4.59880705606552));
#14345=CARTESIAN_POINT('Ctrl Pts',(3.91977655056228,17.6453456436582,4.59485638705045));
#14346=CARTESIAN_POINT('Ctrl Pts',(3.90408240284739,17.6353991351895,4.59243495840567));
#14347=CARTESIAN_POINT('Ctrl Pts',(3.89091287885364,17.6237941840314,4.59));
#14348=CARTESIAN_POINT('Origin',(4.,17.5,4.59));
#14349=CARTESIAN_POINT('',(3.89091287885364,16.9,4.59));
#14350=CARTESIAN_POINT('Origin',(2.9,17.5,2.));
#14351=CARTESIAN_POINT('',(2.5,17.5,2.));
#14352=CARTESIAN_POINT('Origin',(2.9,17.5,2.));
#14353=CARTESIAN_POINT('',(2.5,17.5,5.));
#14354=CARTESIAN_POINT('',(2.5,17.5,2.));
#14355=CARTESIAN_POINT('Origin',(2.9,17.5,5.));
#14356=CARTESIAN_POINT('',(2.5,17.5,2.));
#14357=CARTESIAN_POINT('Origin',(2.9,17.5,2.));
#14358=CARTESIAN_POINT('',(2.675,17.5,2.));
#14359=CARTESIAN_POINT('Origin',(2.9,17.5,2.));
#14360=CARTESIAN_POINT('Origin',(5.1,17.5,2.));
#14361=CARTESIAN_POINT('Origin',(5.1,17.5,5.));
#14362=CARTESIAN_POINT('',(5.5,17.5,2.));
#14363=CARTESIAN_POINT('Origin',(5.1,17.5,2.));
#14364=CARTESIAN_POINT('Origin',(5.1,17.5,2.));
#14365=CARTESIAN_POINT('',(4.875,17.5,2.));
#14366=CARTESIAN_POINT('Origin',(5.1,17.5,2.));
#14367=CARTESIAN_POINT('Origin',(4.,17.5,5.));
#14368=CARTESIAN_POINT('',(2.5,18.,5.));
#14369=CARTESIAN_POINT('',(2.5,18.,5.));
#14370=CARTESIAN_POINT('',(2.5,17.,5.));
#14371=CARTESIAN_POINT('',(2.5,18.,5.));
#14372=CARTESIAN_POINT('',(5.5,17.,5.));
#14373=CARTESIAN_POINT('',(2.5,17.,5.));
#14374=CARTESIAN_POINT('',(5.5,17.,5.));
#14375=CARTESIAN_POINT('',(5.5,18.,5.));
#14376=CARTESIAN_POINT('',(5.5,17.,5.));
#14377=CARTESIAN_POINT('',(5.5,18.,5.));
#14378=CARTESIAN_POINT('Origin',(2.9,17.5,0.9));
#14379=CARTESIAN_POINT('',(2.675,17.5,1.));
#14380=CARTESIAN_POINT('Origin',(2.9,17.5,1.));
#14381=CARTESIAN_POINT('',(2.675,17.5,0.9));
#14382=CARTESIAN_POINT('Origin',(5.1,17.5,0.9));
#14383=CARTESIAN_POINT('',(4.875,17.5,1.));
#14384=CARTESIAN_POINT('Origin',(5.1,17.5,1.));
#14385=CARTESIAN_POINT('',(4.875,17.5,0.9));
#14386=CARTESIAN_POINT('Origin',(4.,16.9,4.));
#14387=CARTESIAN_POINT('',(3.4,17.,4.));
#14388=CARTESIAN_POINT('Origin',(4.,17.,4.));
#14389=CARTESIAN_POINT('',(3.4,18.,4.));
#14390=CARTESIAN_POINT('',(3.4,16.9,4.));
#14391=CARTESIAN_POINT('Origin',(4.,18.,4.));
#14392=CARTESIAN_POINT('Origin',(5.5,18.,1.));
#14393=CARTESIAN_POINT('',(5.5,18.,1.));
#14394=CARTESIAN_POINT('',(2.5,18.,1.));
#14395=CARTESIAN_POINT('',(5.5,18.,1.));
#14396=CARTESIAN_POINT('',(2.5,18.,1.));
#14397=CARTESIAN_POINT('',(5.5,18.,1.));
#14398=CARTESIAN_POINT('Origin',(5.5,17.,1.));
#14399=CARTESIAN_POINT('',(5.5,17.,1.));
#14400=CARTESIAN_POINT('',(5.5,17.,1.));
#14401=CARTESIAN_POINT('',(5.5,17.,1.));
#14402=CARTESIAN_POINT('Origin',(2.5,17.,1.));
#14403=CARTESIAN_POINT('',(2.5,17.,1.));
#14404=CARTESIAN_POINT('',(2.5,17.,1.));
#14405=CARTESIAN_POINT('',(2.5,17.,1.));
#14406=CARTESIAN_POINT('Origin',(2.5,18.,1.));
#14407=CARTESIAN_POINT('',(2.5,18.,1.));
#14408=CARTESIAN_POINT('Origin',(4.,17.5,1.));
#16561=UNCERTAINTY_MEASURE_WITH_UNIT(LENGTH_MEASURE(0.001),#16679,
'DISTANCE_ACCURACY_VALUE',
'Maximum model space distance between geometric entities at asserted c
onnectivities');
#16614=UNCERTAINTY_MEASURE_WITH_UNIT(LENGTH_MEASURE(0.001),#16679,
'DISTANCE_ACCURACY_VALUE',
'Maximum model space distance between geometric entities at asserted c
onnectivities');
#16625=(
GEOMETRIC_REPRESENTATION_CONTEXT(3)
GLOBAL_UNCERTAINTY_ASSIGNED_CONTEXT((#16561))
GLOBAL_UNIT_ASSIGNED_CONTEXT((#16679,#16681,#16682))
REPRESENTATION_CONTEXT('','3D')
);
#16678=(
GEOMETRIC_REPRESENTATION_CONTEXT(3)
GLOBAL_UNCERTAINTY_ASSIGNED_CONTEXT((#16614))
GLOBAL_UNIT_ASSIGNED_CONTEXT((#16679,#16681,#16682))
REPRESENTATION_CONTEXT('','3D')
);
#16679=(
LENGTH_UNIT()
NAMED_UNIT(*)
SI_UNIT(.CENTI.,.METRE.)
);
#16681=(
NAMED_UNIT(*)
PLANE_ANGLE_UNIT()
SI_UNIT($,.RADIAN.)
);
#16682=(
NAMED_UNIT(*)
SI_UNIT($,.STERADIAN.)
SOLID_ANGLE_UNIT()
);
#16693=SHAPE_DEFINITION_REPRESENTATION(#16756,#16920);
#16756=PRODUCT_DEFINITION_SHAPE('',$,#16984);
#16920=SHAPE_REPRESENTATION('',(#9730),#16625);
#16973=PRODUCT_DEFINITION_CONTEXT('part definition',#17164,'design');
#16984=PRODUCT_DEFINITION('Vertical shaft support (1)',
'Vertical shaft support (1)',#17047,#16973);
#17047=PRODUCT_DEFINITION_FORMATION('',$,#17176);
#17164=APPLICATION_CONTEXT(
'Core Data for Automotive Mechanical Design Process');
#17165=PRODUCT_CONTEXT('part definition',#17164,'mechanical');
#17176=PRODUCT('Vertical shaft support (1)','Vertical shaft support (1)',
'Vertical shaft support (1)',(#17165));
#17285=COLOUR_RGB('Grey',0.48,0.52,0.57);
#17286=FILL_AREA_STYLE_COLOUR('',#17285);
#17287=FILL_AREA_STYLE('',(#17286));
#17288=SURFACE_STYLE_FILL_AREA(#17287);
#17289=SURFACE_SIDE_STYLE('',(#17288));
#17290=SURFACE_STYLE_USAGE(.BOTH.,#17289);
#17291=PRESENTATION_STYLE_ASSIGNMENT((#17290));
ENDSEC;
END-ISO-10303-21;
